ISO-10303-21;
HEADER;
/* Generated by software containing ST-Developer
 * from STEP Tools, Inc. (www.steptools.com) 
 */

FILE_DESCRIPTION(
/* description */ ('PAT-003'),
/* implementation_level */ '2;1');

FILE_NAME(
/* name */ 'Captive-nut hand knob.step',
/* time_stamp */ '2026-10-29T15:45:40-07:00',
/* author */ (''),
/* organization */ (''),
/* preprocessor_version */ 'ST-DEVELOPER v20.2',
/* originating_system */ 'Autodesk Translation Framework v15.17.0.0',
/* authorisation */ '');

FILE_SCHEMA (('AUTOMOTIVE_DESIGN { 1 0 10303 214 3 1 1 }'));
ENDSEC;

DATA;
#10=MECHANICAL_DESIGN_GEOMETRIC_PRESENTATION_REPRESENTATION('',(#158),#5761);
#134=SHAPE_REPRESENTATION_RELATIONSHIP('SRR','None',#5829,#146);
#146=ADVANCED_BREP_SHAPE_REPRESENTATION('',(#168),#5760);
#158=STYLED_ITEM('',(#5956),#168);
#168=MANIFOLD_SOLID_BREP('Body1',#3334);
#203=FACE_BOUND('',#734,.T.);
#204=FACE_BOUND('',#748,.T.);
#205=FACE_BOUND('',#751,.T.);
#332=PLANE('',#3748);
#333=PLANE('',#3768);
#334=PLANE('',#3769);
#335=PLANE('',#3770);
#336=PLANE('',#3771);
#337=PLANE('',#3772);
#338=PLANE('',#3773);
#339=PLANE('',#3774);
#340=PLANE('',#3777);
#506=FACE_OUTER_BOUND('',#727,.T.);
#507=FACE_OUTER_BOUND('',#728,.T.);
#508=FACE_OUTER_BOUND('',#729,.T.);
#509=FACE_OUTER_BOUND('',#730,.T.);
#510=FACE_OUTER_BOUND('',#731,.T.);
#511=FACE_OUTER_BOUND('',#732,.T.);
#512=FACE_OUTER_BOUND('',#733,.T.);
#513=FACE_OUTER_BOUND('',#735,.T.);
#514=FACE_OUTER_BOUND('',#736,.T.);
#515=FACE_OUTER_BOUND('',#737,.T.);
#516=FACE_OUTER_BOUND('',#738,.T.);
#517=FACE_OUTER_BOUND('',#739,.T.);
#518=FACE_OUTER_BOUND('',#740,.T.);
#519=FACE_OUTER_BOUND('',#741,.T.);
#520=FACE_OUTER_BOUND('',#742,.T.);
#521=FACE_OUTER_BOUND('',#743,.T.);
#522=FACE_OUTER_BOUND('',#744,.T.);
#523=FACE_OUTER_BOUND('',#745,.T.);
#524=FACE_OUTER_BOUND('',#746,.T.);
#525=FACE_OUTER_BOUND('',#747,.T.);
#526=FACE_OUTER_BOUND('',#749,.T.);
#527=FACE_OUTER_BOUND('',#750,.T.);
#727=EDGE_LOOP('',(#2980,#2981,#2982,#2983));
#728=EDGE_LOOP('',(#2984,#2985,#2986,#2987));
#729=EDGE_LOOP('',(#2988,#2989,#2990,#2991));
#730=EDGE_LOOP('',(#2992,#2993,#2994,#2995));
#731=EDGE_LOOP('',(#2996,#2997,#2998,#2999));
#732=EDGE_LOOP('',(#3000,#3001,#3002,#3003));
#733=EDGE_LOOP('',(#3004,#3005,#3006,#3007,#3008,#3009,#3010,#3011,#3012,
#3013,#3014,#3015));
#734=EDGE_LOOP('',(#3016));
#735=EDGE_LOOP('',(#3017,#3018,#3019,#3020));
#736=EDGE_LOOP('',(#3021,#3022,#3023,#3024));
#737=EDGE_LOOP('',(#3025,#3026,#3027,#3028));
#738=EDGE_LOOP('',(#3029,#3030,#3031,#3032));
#739=EDGE_LOOP('',(#3033,#3034,#3035,#3036));
#740=EDGE_LOOP('',(#3037,#3038,#3039,#3040));
#741=EDGE_LOOP('',(#3041,#3042,#3043,#3044));
#742=EDGE_LOOP('',(#3045,#3046,#3047,#3048));
#743=EDGE_LOOP('',(#3049,#3050,#3051,#3052));
#744=EDGE_LOOP('',(#3053,#3054,#3055,#3056));
#745=EDGE_LOOP('',(#3057,#3058,#3059,#3060));
#746=EDGE_LOOP('',(#3061,#3062,#3063,#3064));
#747=EDGE_LOOP('',(#3065,#3066,#3067,#3068,#3069,#3070));
#748=EDGE_LOOP('',(#3071));
#749=EDGE_LOOP('',(#3072,#3073,#3074,#3075));
#750=EDGE_LOOP('',(#3076,#3077,#3078,#3079,#3080,#3081,#3082,#3083,#3084,
#3085,#3086,#3087));
#751=EDGE_LOOP('',(#3088,#3089,#3090,#3091,#3092,#3093));
#1043=LINE('',#5607,#1365);
#1044=LINE('',#5611,#1366);
#1045=LINE('',#5616,#1367);
#1046=LINE('',#5620,#1368);
#1047=LINE('',#5625,#1369);
#1048=LINE('',#5629,#1370);
#1049=LINE('',#5634,#1371);
#1050=LINE('',#5638,#1372);
#1051=LINE('',#5643,#1373);
#1052=LINE('',#5647,#1374);
#1053=LINE('',#5652,#1375);
#1054=LINE('',#5656,#1376);
#1055=LINE('',#5682,#1377);
#1056=LINE('',#5684,#1378);
#1057=LINE('',#5686,#1379);
#1058=LINE('',#5687,#1380);
#1059=LINE('',#5690,#1381);
#1060=LINE('',#5692,#1382);
#1061=LINE('',#5693,#1383);
#1062=LINE('',#5696,#1384);
#1063=LINE('',#5698,#1385);
#1064=LINE('',#5699,#1386);
#1065=LINE('',#5702,#1387);
#1066=LINE('',#5704,#1388);
#1067=LINE('',#5705,#1389);
#1068=LINE('',#5708,#1390);
#1069=LINE('',#5710,#1391);
#1070=LINE('',#5711,#1392);
#1071=LINE('',#5713,#1393);
#1072=LINE('',#5714,#1394);
#1073=LINE('',#5719,#1395);
#1365=VECTOR('',#4604,1.);
#1366=VECTOR('',#4607,1.);
#1367=VECTOR('',#4612,1.);
#1368=VECTOR('',#4615,1.);
#1369=VECTOR('',#4620,1.);
#1370=VECTOR('',#4623,1.);
#1371=VECTOR('',#4628,1.);
#1372=VECTOR('',#4631,1.);
#1373=VECTOR('',#4636,1.);
#1374=VECTOR('',#4639,1.);
#1375=VECTOR('',#4644,1.);
#1376=VECTOR('',#4647,1.);
#1377=VECTOR('',#4692,1.);
#1378=VECTOR('',#4693,1.);
#1379=VECTOR('',#4694,1.);
#1380=VECTOR('',#4695,1.);
#1381=VECTOR('',#4698,1.);
#1382=VECTOR('',#4699,1.);
#1383=VECTOR('',#4700,1.);
#1384=VECTOR('',#4703,1.);
#1385=VECTOR('',#4704,1.);
#1386=VECTOR('',#4705,1.);
#1387=VECTOR('',#4708,1.);
#1388=VECTOR('',#4709,1.);
#1389=VECTOR('',#4710,1.);
#1390=VECTOR('',#4713,1.);
#1391=VECTOR('',#4714,1.);
#1392=VECTOR('',#4715,1.);
#1393=VECTOR('',#4718,1.);
#1394=VECTOR('',#4719,1.);
#1395=VECTOR('',#4726,0.425);
#1466=CIRCLE('',#3731,0.4);
#1467=CIRCLE('',#3732,0.4);
#1468=CIRCLE('',#3734,0.4);
#1469=CIRCLE('',#3735,0.4);
#1470=CIRCLE('',#3737,0.4);
#1471=CIRCLE('',#3738,0.4);
#1472=CIRCLE('',#3740,0.4);
#1473=CIRCLE('',#3741,0.4);
#1474=CIRCLE('',#3743,0.4);
#1475=CIRCLE('',#3744,0.4);
#1476=CIRCLE('',#3746,0.4);
#1477=CIRCLE('',#3747,0.4);
#1478=CIRCLE('',#3749,1.8);
#1479=CIRCLE('',#3750,1.8);
#1480=CIRCLE('',#3751,1.8);
#1481=CIRCLE('',#3752,1.8);
#1482=CIRCLE('',#3753,1.8);
#1483=CIRCLE('',#3754,1.8);
#1484=CIRCLE('',#3755,0.425);
#1485=CIRCLE('',#3757,1.8);
#1486=CIRCLE('',#3759,1.8);
#1487=CIRCLE('',#3761,1.8);
#1488=CIRCLE('',#3763,1.8);
#1489=CIRCLE('',#3765,1.8);
#1490=CIRCLE('',#3767,1.8);
#1491=CIRCLE('',#3775,0.425);
#1742=VERTEX_POINT('',#5605);
#1743=VERTEX_POINT('',#5606);
#1744=VERTEX_POINT('',#5608);
#1745=VERTEX_POINT('',#5610);
#1746=VERTEX_POINT('',#5614);
#1747=VERTEX_POINT('',#5615);
#1748=VERTEX_POINT('',#5617);
#1749=VERTEX_POINT('',#5619);
#1750=VERTEX_POINT('',#5623);
#1751=VERTEX_POINT('',#5624);
#1752=VERTEX_POINT('',#5626);
#1753=VERTEX_POINT('',#5628);
#1754=VERTEX_POINT('',#5632);
#1755=VERTEX_POINT('',#5633);
#1756=VERTEX_POINT('',#5635);
#1757=VERTEX_POINT('',#5637);
#1758=VERTEX_POINT('',#5641);
#1759=VERTEX_POINT('',#5642);
#1760=VERTEX_POINT('',#5644);
#1761=VERTEX_POINT('',#5646);
#1762=VERTEX_POINT('',#5650);
#1763=VERTEX_POINT('',#5651);
#1764=VERTEX_POINT('',#5653);
#1765=VERTEX_POINT('',#5655);
#1766=VERTEX_POINT('',#5665);
#1767=VERTEX_POINT('',#5680);
#1768=VERTEX_POINT('',#5681);
#1769=VERTEX_POINT('',#5683);
#1770=VERTEX_POINT('',#5685);
#1771=VERTEX_POINT('',#5689);
#1772=VERTEX_POINT('',#5691);
#1773=VERTEX_POINT('',#5695);
#1774=VERTEX_POINT('',#5697);
#1775=VERTEX_POINT('',#5701);
#1776=VERTEX_POINT('',#5703);
#1777=VERTEX_POINT('',#5707);
#1778=VERTEX_POINT('',#5709);
#1779=VERTEX_POINT('',#5716);
#2161=EDGE_CURVE('',#1742,#1743,#1043,.T.);
#2162=EDGE_CURVE('',#1744,#1742,#1466,.T.);
#2163=EDGE_CURVE('',#1745,#1744,#1044,.T.);
#2164=EDGE_CURVE('',#1743,#1745,#1467,.T.);
#2165=EDGE_CURVE('',#1746,#1747,#1045,.T.);
#2166=EDGE_CURVE('',#1748,#1746,#1468,.T.);
#2167=EDGE_CURVE('',#1749,#1748,#1046,.T.);
#2168=EDGE_CURVE('',#1747,#1749,#1469,.T.);
#2169=EDGE_CURVE('',#1750,#1751,#1047,.T.);
#2170=EDGE_CURVE('',#1752,#1750,#1470,.T.);
#2171=EDGE_CURVE('',#1753,#1752,#1048,.T.);
#2172=EDGE_CURVE('',#1751,#1753,#1471,.T.);
#2173=EDGE_CURVE('',#1754,#1755,#1049,.T.);
#2174=EDGE_CURVE('',#1756,#1754,#1472,.T.);
#2175=EDGE_CURVE('',#1757,#1756,#1050,.T.);
#2176=EDGE_CURVE('',#1755,#1757,#1473,.T.);
#2177=EDGE_CURVE('',#1758,#1759,#1051,.T.);
#2178=EDGE_CURVE('',#1760,#1758,#1474,.T.);
#2179=EDGE_CURVE('',#1761,#1760,#1052,.T.);
#2180=EDGE_CURVE('',#1759,#1761,#1475,.T.);
#2181=EDGE_CURVE('',#1762,#1763,#1053,.T.);
#2182=EDGE_CURVE('',#1764,#1762,#1476,.T.);
#2183=EDGE_CURVE('',#1765,#1764,#1054,.T.);
#2184=EDGE_CURVE('',#1763,#1765,#1477,.T.);
#2185=EDGE_CURVE('',#1742,#1764,#1478,.T.);
#2186=EDGE_CURVE('',#1762,#1747,#1479,.T.);
#2187=EDGE_CURVE('',#1749,#1752,#1480,.T.);
#2188=EDGE_CURVE('',#1750,#1756,#1481,.T.);
#2189=EDGE_CURVE('',#1754,#1760,#1482,.T.);
#2190=EDGE_CURVE('',#1758,#1744,#1483,.T.);
#2191=EDGE_CURVE('',#1766,#1766,#1484,.T.);
#2192=EDGE_CURVE('',#1755,#1761,#1485,.T.);
#2193=EDGE_CURVE('',#1751,#1757,#1486,.T.);
#2194=EDGE_CURVE('',#1763,#1746,#1487,.T.);
#2195=EDGE_CURVE('',#1748,#1753,#1488,.T.);
#2196=EDGE_CURVE('',#1743,#1765,#1489,.T.);
#2197=EDGE_CURVE('',#1759,#1745,#1490,.T.);
#2198=EDGE_CURVE('',#1767,#1768,#1055,.T.);
#2199=EDGE_CURVE('',#1767,#1769,#1056,.T.);
#2200=EDGE_CURVE('',#1769,#1770,#1057,.T.);
#2201=EDGE_CURVE('',#1768,#1770,#1058,.T.);
#2202=EDGE_CURVE('',#1768,#1771,#1059,.T.);
#2203=EDGE_CURVE('',#1770,#1772,#1060,.T.);
#2204=EDGE_CURVE('',#1771,#1772,#1061,.T.);
#2205=EDGE_CURVE('',#1771,#1773,#1062,.T.);
#2206=EDGE_CURVE('',#1772,#1774,#1063,.T.);
#2207=EDGE_CURVE('',#1773,#1774,#1064,.T.);
#2208=EDGE_CURVE('',#1773,#1775,#1065,.T.);
#2209=EDGE_CURVE('',#1774,#1776,#1066,.T.);
#2210=EDGE_CURVE('',#1775,#1776,#1067,.T.);
#2211=EDGE_CURVE('',#1777,#1767,#1068,.T.);
#2212=EDGE_CURVE('',#1777,#1778,#1069,.T.);
#2213=EDGE_CURVE('',#1778,#1769,#1070,.T.);
#2214=EDGE_CURVE('',#1775,#1777,#1071,.T.);
#2215=EDGE_CURVE('',#1776,#1778,#1072,.T.);
#2216=EDGE_CURVE('',#1779,#1779,#1491,.T.);
#2217=EDGE_CURVE('',#1766,#1779,#1073,.T.);
#2980=ORIENTED_EDGE('',*,*,#2161,.F.);
#2981=ORIENTED_EDGE('',*,*,#2162,.F.);
#2982=ORIENTED_EDGE('',*,*,#2163,.F.);
#2983=ORIENTED_EDGE('',*,*,#2164,.F.);
#2984=ORIENTED_EDGE('',*,*,#2165,.F.);
#2985=ORIENTED_EDGE('',*,*,#2166,.F.);
#2986=ORIENTED_EDGE('',*,*,#2167,.F.);
#2987=ORIENTED_EDGE('',*,*,#2168,.F.);
#2988=ORIENTED_EDGE('',*,*,#2169,.F.);
#2989=ORIENTED_EDGE('',*,*,#2170,.F.);
#2990=ORIENTED_EDGE('',*,*,#2171,.F.);
#2991=ORIENTED_EDGE('',*,*,#2172,.F.);
#2992=ORIENTED_EDGE('',*,*,#2173,.F.);
#2993=ORIENTED_EDGE('',*,*,#2174,.F.);
#2994=ORIENTED_EDGE('',*,*,#2175,.F.);
#2995=ORIENTED_EDGE('',*,*,#2176,.F.);
#2996=ORIENTED_EDGE('',*,*,#2177,.F.);
#2997=ORIENTED_EDGE('',*,*,#2178,.F.);
#2998=ORIENTED_EDGE('',*,*,#2179,.F.);
#2999=ORIENTED_EDGE('',*,*,#2180,.F.);
#3000=ORIENTED_EDGE('',*,*,#2181,.F.);
#3001=ORIENTED_EDGE('',*,*,#2182,.F.);
#3002=ORIENTED_EDGE('',*,*,#2183,.F.);
#3003=ORIENTED_EDGE('',*,*,#2184,.F.);
#3004=ORIENTED_EDGE('',*,*,#2162,.T.);
#3005=ORIENTED_EDGE('',*,*,#2185,.T.);
#3006=ORIENTED_EDGE('',*,*,#2182,.T.);
#3007=ORIENTED_EDGE('',*,*,#2186,.T.);
#3008=ORIENTED_EDGE('',*,*,#2168,.T.);
#3009=ORIENTED_EDGE('',*,*,#2187,.T.);
#3010=ORIENTED_EDGE('',*,*,#2170,.T.);
#3011=ORIENTED_EDGE('',*,*,#2188,.T.);
#3012=ORIENTED_EDGE('',*,*,#2174,.T.);
#3013=ORIENTED_EDGE('',*,*,#2189,.T.);
#3014=ORIENTED_EDGE('',*,*,#2178,.T.);
#3015=ORIENTED_EDGE('',*,*,#2190,.T.);
#3016=ORIENTED_EDGE('',*,*,#2191,.T.);
#3017=ORIENTED_EDGE('',*,*,#2173,.T.);
#3018=ORIENTED_EDGE('',*,*,#2192,.T.);
#3019=ORIENTED_EDGE('',*,*,#2179,.T.);
#3020=ORIENTED_EDGE('',*,*,#2189,.F.);
#3021=ORIENTED_EDGE('',*,*,#2169,.T.);
#3022=ORIENTED_EDGE('',*,*,#2193,.T.);
#3023=ORIENTED_EDGE('',*,*,#2175,.T.);
#3024=ORIENTED_EDGE('',*,*,#2188,.F.);
#3025=ORIENTED_EDGE('',*,*,#2165,.T.);
#3026=ORIENTED_EDGE('',*,*,#2186,.F.);
#3027=ORIENTED_EDGE('',*,*,#2181,.T.);
#3028=ORIENTED_EDGE('',*,*,#2194,.T.);
#3029=ORIENTED_EDGE('',*,*,#2167,.T.);
#3030=ORIENTED_EDGE('',*,*,#2195,.T.);
#3031=ORIENTED_EDGE('',*,*,#2171,.T.);
#3032=ORIENTED_EDGE('',*,*,#2187,.F.);
#3033=ORIENTED_EDGE('',*,*,#2161,.T.);
#3034=ORIENTED_EDGE('',*,*,#2196,.T.);
#3035=ORIENTED_EDGE('',*,*,#2183,.T.);
#3036=ORIENTED_EDGE('',*,*,#2185,.F.);
#3037=ORIENTED_EDGE('',*,*,#2163,.T.);
#3038=ORIENTED_EDGE('',*,*,#2190,.F.);
#3039=ORIENTED_EDGE('',*,*,#2177,.T.);
#3040=ORIENTED_EDGE('',*,*,#2197,.T.);
#3041=ORIENTED_EDGE('',*,*,#2198,.F.);
#3042=ORIENTED_EDGE('',*,*,#2199,.T.);
#3043=ORIENTED_EDGE('',*,*,#2200,.T.);
#3044=ORIENTED_EDGE('',*,*,#2201,.F.);
#3045=ORIENTED_EDGE('',*,*,#2202,.F.);
#3046=ORIENTED_EDGE('',*,*,#2201,.T.);
#3047=ORIENTED_EDGE('',*,*,#2203,.T.);
#3048=ORIENTED_EDGE('',*,*,#2204,.F.);
#3049=ORIENTED_EDGE('',*,*,#2205,.F.);
#3050=ORIENTED_EDGE('',*,*,#2204,.T.);
#3051=ORIENTED_EDGE('',*,*,#2206,.T.);
#3052=ORIENTED_EDGE('',*,*,#2207,.F.);
#3053=ORIENTED_EDGE('',*,*,#2208,.F.);
#3054=ORIENTED_EDGE('',*,*,#2207,.T.);
#3055=ORIENTED_EDGE('',*,*,#2209,.T.);
#3056=ORIENTED_EDGE('',*,*,#2210,.F.);
#3057=ORIENTED_EDGE('',*,*,#2211,.F.);
#3058=ORIENTED_EDGE('',*,*,#2212,.T.);
#3059=ORIENTED_EDGE('',*,*,#2213,.T.);
#3060=ORIENTED_EDGE('',*,*,#2199,.F.);
#3061=ORIENTED_EDGE('',*,*,#2214,.F.);
#3062=ORIENTED_EDGE('',*,*,#2210,.T.);
#3063=ORIENTED_EDGE('',*,*,#2215,.T.);
#3064=ORIENTED_EDGE('',*,*,#2212,.F.);
#3065=ORIENTED_EDGE('',*,*,#2215,.F.);
#3066=ORIENTED_EDGE('',*,*,#2209,.F.);
#3067=ORIENTED_EDGE('',*,*,#2206,.F.);
#3068=ORIENTED_EDGE('',*,*,#2203,.F.);
#3069=ORIENTED_EDGE('',*,*,#2200,.F.);
#3070=ORIENTED_EDGE('',*,*,#2213,.F.);
#3071=ORIENTED_EDGE('',*,*,#2216,.F.);
#3072=ORIENTED_EDGE('',*,*,#2191,.F.);
#3073=ORIENTED_EDGE('',*,*,#2217,.T.);
#3074=ORIENTED_EDGE('',*,*,#2216,.T.);
#3075=ORIENTED_EDGE('',*,*,#2217,.F.);
#3076=ORIENTED_EDGE('',*,*,#2164,.T.);
#3077=ORIENTED_EDGE('',*,*,#2197,.F.);
#3078=ORIENTED_EDGE('',*,*,#2180,.T.);
#3079=ORIENTED_EDGE('',*,*,#2192,.F.);
#3080=ORIENTED_EDGE('',*,*,#2176,.T.);
#3081=ORIENTED_EDGE('',*,*,#2193,.F.);
#3082=ORIENTED_EDGE('',*,*,#2172,.T.);
#3083=ORIENTED_EDGE('',*,*,#2195,.F.);
#3084=ORIENTED_EDGE('',*,*,#2166,.T.);
#3085=ORIENTED_EDGE('',*,*,#2194,.F.);
#3086=ORIENTED_EDGE('',*,*,#2184,.T.);
#3087=ORIENTED_EDGE('',*,*,#2196,.F.);
#3088=ORIENTED_EDGE('',*,*,#2208,.T.);
#3089=ORIENTED_EDGE('',*,*,#2214,.T.);
#3090=ORIENTED_EDGE('',*,*,#2211,.T.);
#3091=ORIENTED_EDGE('',*,*,#2198,.T.);
#3092=ORIENTED_EDGE('',*,*,#2202,.T.);
#3093=ORIENTED_EDGE('',*,*,#2205,.T.);
#3121=CYLINDRICAL_SURFACE('',#3730,0.4);
#3122=CYLINDRICAL_SURFACE('',#3733,0.4);
#3123=CYLINDRICAL_SURFACE('',#3736,0.4);
#3124=CYLINDRICAL_SURFACE('',#3739,0.4);
#3125=CYLINDRICAL_SURFACE('',#3742,0.4);
#3126=CYLINDRICAL_SURFACE('',#3745,0.4);
#3127=CYLINDRICAL_SURFACE('',#3756,1.8);
#3128=CYLINDRICAL_SURFACE('',#3758,1.8);
#3129=CYLINDRICAL_SURFACE('',#3760,1.8);
#3130=CYLINDRICAL_SURFACE('',#3762,1.8);
#3131=CYLINDRICAL_SURFACE('',#3764,1.8);
#3132=CYLINDRICAL_SURFACE('',#3766,1.8);
#3133=CYLINDRICAL_SURFACE('',#3776,0.425);
#3299=ADVANCED_FACE('',(#506),#3121,.F.);
#3300=ADVANCED_FACE('',(#507),#3122,.F.);
#3301=ADVANCED_FACE('',(#508),#3123,.F.);
#3302=ADVANCED_FACE('',(#509),#3124,.F.);
#3303=ADVANCED_FACE('',(#510),#3125,.F.);
#3304=ADVANCED_FACE('',(#511),#3126,.F.);
#3305=ADVANCED_FACE('',(#512,#203),#332,.T.);
#3306=ADVANCED_FACE('',(#513),#3127,.T.);
#3307=ADVANCED_FACE('',(#514),#3128,.T.);
#3308=ADVANCED_FACE('',(#515),#3129,.T.);
#3309=ADVANCED_FACE('',(#516),#3130,.T.);
#3310=ADVANCED_FACE('',(#517),#3131,.T.);
#3311=ADVANCED_FACE('',(#518),#3132,.T.);
#3312=ADVANCED_FACE('',(#519),#333,.F.);
#3313=ADVANCED_FACE('',(#520),#334,.F.);
#3314=ADVANCED_FACE('',(#521),#335,.F.);
#3315=ADVANCED_FACE('',(#522),#336,.F.);
#3316=ADVANCED_FACE('',(#523),#337,.F.);
#3317=ADVANCED_FACE('',(#524),#338,.F.);
#3318=ADVANCED_FACE('',(#525,#204),#339,.F.);
#3319=ADVANCED_FACE('',(#526),#3133,.F.);
#3320=ADVANCED_FACE('',(#527,#205),#340,.F.);
#3334=CLOSED_SHELL('',(#3299,#3300,#3301,#3302,#3303,#3304,#3305,#3306,
#3307,#3308,#3309,#3310,#3311,#3312,#3313,#3314,#3315,#3316,#3317,#3318,
#3319,#3320));
#3729=AXIS2_PLACEMENT_3D('',#5603,#4600,#4601);
#3730=AXIS2_PLACEMENT_3D('',#5604,#4602,#4603);
#3731=AXIS2_PLACEMENT_3D('',#5609,#4605,#4606);
#3732=AXIS2_PLACEMENT_3D('',#5612,#4608,#4609);
#3733=AXIS2_PLACEMENT_3D('',#5613,#4610,#4611);
#3734=AXIS2_PLACEMENT_3D('',#5618,#4613,#4614);
#3735=AXIS2_PLACEMENT_3D('',#5621,#4616,#4617);
#3736=AXIS2_PLACEMENT_3D('',#5622,#4618,#4619);
#3737=AXIS2_PLACEMENT_3D('',#5627,#4621,#4622);
#3738=AXIS2_PLACEMENT_3D('',#5630,#4624,#4625);
#3739=AXIS2_PLACEMENT_3D('',#5631,#4626,#4627);
#3740=AXIS2_PLACEMENT_3D('',#5636,#4629,#4630);
#3741=AXIS2_PLACEMENT_3D('',#5639,#4632,#4633);
#3742=AXIS2_PLACEMENT_3D('',#5640,#4634,#4635);
#3743=AXIS2_PLACEMENT_3D('',#5645,#4637,#4638);
#3744=AXIS2_PLACEMENT_3D('',#5648,#4640,#4641);
#3745=AXIS2_PLACEMENT_3D('',#5649,#4642,#4643);
#3746=AXIS2_PLACEMENT_3D('',#5654,#4645,#4646);
#3747=AXIS2_PLACEMENT_3D('',#5657,#4648,#4649);
#3748=AXIS2_PLACEMENT_3D('',#5658,#4650,#4651);
#3749=AXIS2_PLACEMENT_3D('',#5659,#4652,#4653);
#3750=AXIS2_PLACEMENT_3D('',#5660,#4654,#4655);
#3751=AXIS2_PLACEMENT_3D('',#5661,#4656,#4657);
#3752=AXIS2_PLACEMENT_3D('',#5662,#4658,#4659);
#3753=AXIS2_PLACEMENT_3D('',#5663,#4660,#4661);
#3754=AXIS2_PLACEMENT_3D('',#5664,#4662,#4663);
#3755=AXIS2_PLACEMENT_3D('',#5666,#4664,#4665);
#3756=AXIS2_PLACEMENT_3D('',#5667,#4666,#4667);
#3757=AXIS2_PLACEMENT_3D('',#5668,#4668,#4669);
#3758=AXIS2_PLACEMENT_3D('',#5669,#4670,#4671);
#3759=AXIS2_PLACEMENT_3D('',#5670,#4672,#4673);
#3760=AXIS2_PLACEMENT_3D('',#5671,#4674,#4675);
#3761=AXIS2_PLACEMENT_3D('',#5672,#4676,#4677);
#3762=AXIS2_PLACEMENT_3D('',#5673,#4678,#4679);
#3763=AXIS2_PLACEMENT_3D('',#5674,#4680,#4681);
#3764=AXIS2_PLACEMENT_3D('',#5675,#4682,#4683);
#3765=AXIS2_PLACEMENT_3D('',#5676,#4684,#4685);
#3766=AXIS2_PLACEMENT_3D('',#5677,#4686,#4687);
#3767=AXIS2_PLACEMENT_3D('',#5678,#4688,#4689);
#3768=AXIS2_PLACEMENT_3D('',#5679,#4690,#4691);
#3769=AXIS2_PLACEMENT_3D('',#5688,#4696,#4697);
#3770=AXIS2_PLACEMENT_3D('',#5694,#4701,#4702);
#3771=AXIS2_PLACEMENT_3D('',#5700,#4706,#4707);
#3772=AXIS2_PLACEMENT_3D('',#5706,#4711,#4712);
#3773=AXIS2_PLACEMENT_3D('',#5712,#4716,#4717);
#3774=AXIS2_PLACEMENT_3D('',#5715,#4720,#4721);
#3775=AXIS2_PLACEMENT_3D('',#5717,#4722,#4723);
#3776=AXIS2_PLACEMENT_3D('',#5718,#4724,#4725);
#3777=AXIS2_PLACEMENT_3D('',#5720,#4727,#4728);
#4600=DIRECTION('axis',(0.,0.,1.));
#4601=DIRECTION('refdir',(1.,0.,0.));
#4602=DIRECTION('center_axis',(0.,0.,1.));
#4603=DIRECTION('ref_axis',(1.,0.,0.));
#4604=DIRECTION('',(0.,0.,-1.));
#4605=DIRECTION('center_axis',(0.,0.,-1.));
#4606=DIRECTION('ref_axis',(1.,0.,0.));
#4607=DIRECTION('',(0.,0.,1.));
#4608=DIRECTION('center_axis',(0.,0.,1.));
#4609=DIRECTION('ref_axis',(1.,0.,0.));
#4610=DIRECTION('center_axis',(0.,0.,1.));
#4611=DIRECTION('ref_axis',(-1.,-1.22464679914735E-16,0.));
#4612=DIRECTION('',(0.,0.,1.));
#4613=DIRECTION('center_axis',(0.,0.,1.));
#4614=DIRECTION('ref_axis',(1.,0.,0.));
#4615=DIRECTION('',(0.,0.,-1.));
#4616=DIRECTION('center_axis',(0.,0.,-1.));
#4617=DIRECTION('ref_axis',(1.,0.,0.));
#4618=DIRECTION('center_axis',(0.,0.,1.));
#4619=DIRECTION('ref_axis',(1.,0.,0.));
#4620=DIRECTION('',(0.,0.,-1.));
#4621=DIRECTION('center_axis',(0.,0.,-1.));
#4622=DIRECTION('ref_axis',(1.,0.,0.));
#4623=DIRECTION('',(0.,0.,1.));
#4624=DIRECTION('center_axis',(0.,0.,1.));
#4625=DIRECTION('ref_axis',(1.,0.,0.));
#4626=DIRECTION('center_axis',(0.,0.,1.));
#4627=DIRECTION('ref_axis',(1.,0.,0.));
#4628=DIRECTION('',(0.,0.,-1.));
#4629=DIRECTION('center_axis',(0.,0.,-1.));
#4630=DIRECTION('ref_axis',(1.,0.,0.));
#4631=DIRECTION('',(0.,0.,1.));
#4632=DIRECTION('center_axis',(0.,0.,1.));
#4633=DIRECTION('ref_axis',(1.,0.,0.));
#4634=DIRECTION('center_axis',(0.,0.,1.));
#4635=DIRECTION('ref_axis',(1.,0.,0.));
#4636=DIRECTION('',(0.,0.,-1.));
#4637=DIRECTION('center_axis',(0.,0.,-1.));
#4638=DIRECTION('ref_axis',(1.,0.,0.));
#4639=DIRECTION('',(0.,0.,1.));
#4640=DIRECTION('center_axis',(0.,0.,1.));
#4641=DIRECTION('ref_axis',(1.,0.,0.));
#4642=DIRECTION('center_axis',(0.,0.,1.));
#4643=DIRECTION('ref_axis',(1.,0.,0.));
#4644=DIRECTION('',(0.,0.,-1.));
#4645=DIRECTION('center_axis',(0.,0.,-1.));
#4646=DIRECTION('ref_axis',(1.,0.,0.));
#4647=DIRECTION('',(0.,0.,1.));
#4648=DIRECTION('center_axis',(0.,0.,1.));
#4649=DIRECTION('ref_axis',(1.,0.,0.));
#4650=DIRECTION('center_axis',(0.,0.,1.));
#4651=DIRECTION('ref_axis',(1.,0.,0.));
#4652=DIRECTION('center_axis',(0.,0.,1.));
#4653=DIRECTION('ref_axis',(1.,0.,0.));
#4654=DIRECTION('center_axis',(0.,0.,1.));
#4655=DIRECTION('ref_axis',(1.,0.,0.));
#4656=DIRECTION('center_axis',(0.,0.,1.));
#4657=DIRECTION('ref_axis',(1.,0.,0.));
#4658=DIRECTION('center_axis',(0.,0.,1.));
#4659=DIRECTION('ref_axis',(1.,0.,0.));
#4660=DIRECTION('center_axis',(0.,0.,1.));
#4661=DIRECTION('ref_axis',(1.,0.,0.));
#4662=DIRECTION('center_axis',(0.,0.,1.));
#4663=DIRECTION('ref_axis',(1.,0.,0.));
#4664=DIRECTION('center_axis',(0.,0.,-1.));
#4665=DIRECTION('ref_axis',(1.,0.,0.));
#4666=DIRECTION('center_axis',(0.,0.,1.));
#4667=DIRECTION('ref_axis',(1.,0.,0.));
#4668=DIRECTION('center_axis',(0.,0.,1.));
#4669=DIRECTION('ref_axis',(1.,0.,0.));
#4670=DIRECTION('center_axis',(0.,0.,1.));
#4671=DIRECTION('ref_axis',(1.,0.,0.));
#4672=DIRECTION('center_axis',(0.,0.,1.));
#4673=DIRECTION('ref_axis',(1.,0.,0.));
#4674=DIRECTION('center_axis',(0.,0.,1.));
#4675=DIRECTION('ref_axis',(1.,0.,0.));
#4676=DIRECTION('center_axis',(0.,0.,1.));
#4677=DIRECTION('ref_axis',(1.,0.,0.));
#4678=DIRECTION('center_axis',(0.,0.,1.));
#4679=DIRECTION('ref_axis',(1.,0.,0.));
#4680=DIRECTION('center_axis',(0.,0.,1.));
#4681=DIRECTION('ref_axis',(1.,0.,0.));
#4682=DIRECTION('center_axis',(0.,0.,1.));
#4683=DIRECTION('ref_axis',(1.,0.,0.));
#4684=DIRECTION('center_axis',(0.,0.,1.));
#4685=DIRECTION('ref_axis',(1.,0.,0.));
#4686=DIRECTION('center_axis',(0.,0.,1.));
#4687=DIRECTION('ref_axis',(1.,0.,0.));
#4688=DIRECTION('center_axis',(0.,0.,1.));
#4689=DIRECTION('ref_axis',(1.,0.,0.));
#4690=DIRECTION('center_axis',(0.,1.,0.));
#4691=DIRECTION('ref_axis',(-1.,0.,0.));
#4692=DIRECTION('',(-1.,0.,0.));
#4693=DIRECTION('',(0.,0.,1.));
#4694=DIRECTION('',(-1.,0.,0.));
#4695=DIRECTION('',(0.,0.,1.));
#4696=DIRECTION('center_axis',(-0.866025403784438,0.500000000000001,0.));
#4697=DIRECTION('ref_axis',(-0.500000000000001,-0.866025403784438,0.));
#4698=DIRECTION('',(-0.500000000000001,-0.866025403784438,0.));
#4699=DIRECTION('',(-0.500000000000001,-0.866025403784438,0.));
#4700=DIRECTION('',(0.,0.,1.));
#4701=DIRECTION('center_axis',(-0.866025403784439,-0.5,0.));
#4702=DIRECTION('ref_axis',(0.5,-0.866025403784439,0.));
#4703=DIRECTION('',(0.5,-0.866025403784439,0.));
#4704=DIRECTION('',(0.5,-0.866025403784439,0.));
#4705=DIRECTION('',(0.,0.,1.));
#4706=DIRECTION('center_axis',(0.,-1.,0.));
#4707=DIRECTION('ref_axis',(1.,0.,0.));
#4708=DIRECTION('',(1.,0.,0.));
#4709=DIRECTION('',(1.,0.,0.));
#4710=DIRECTION('',(0.,0.,1.));
#4711=DIRECTION('center_axis',(0.866025403784439,0.5,0.));
#4712=DIRECTION('ref_axis',(-0.5,0.866025403784439,0.));
#4713=DIRECTION('',(-0.5,0.866025403784439,0.));
#4714=DIRECTION('',(0.,0.,1.));
#4715=DIRECTION('',(-0.5,0.866025403784439,0.));
#4716=DIRECTION('center_axis',(0.866025403784439,-0.5,0.));
#4717=DIRECTION('ref_axis',(0.5,0.866025403784439,0.));
#4718=DIRECTION('',(0.5,0.866025403784439,0.));
#4719=DIRECTION('',(0.5,0.866025403784439,0.));
#4720=DIRECTION('center_axis',(0.,0.,1.));
#4721=DIRECTION('ref_axis',(1.,0.,0.));
#4722=DIRECTION('center_axis',(0.,0.,-1.));
#4723=DIRECTION('ref_axis',(1.,0.,0.));
#4724=DIRECTION('center_axis',(0.,0.,1.));
#4725=DIRECTION('ref_axis',(1.,0.,0.));
#4726=DIRECTION('',(0.,0.,-1.));
#4727=DIRECTION('center_axis',(0.,0.,1.));
#4728=DIRECTION('ref_axis',(1.,0.,0.));
#5603=CARTESIAN_POINT('',(0.,0.,0.));
#5604=CARTESIAN_POINT('Origin',(6.5,-5.73205080756888,7.22132034));
#5605=CARTESIAN_POINT('',(6.89841665441537,-5.69649564641799,8.48132034));
#5606=CARTESIAN_POINT('',(6.89841665441537,-5.69649564641799,7.28132034));
#5607=CARTESIAN_POINT('',(6.89841665441537,-5.69649564641799,7.22132034));
#5608=CARTESIAN_POINT('',(6.33158334558463,-5.36923428297892,8.48132034));
#5609=CARTESIAN_POINT('Origin',(6.5,-5.73205080756888,8.48132034));
#5610=CARTESIAN_POINT('',(6.33158334558463,-5.36923428297892,7.28132034));
#5611=CARTESIAN_POINT('',(6.33158334558463,-5.36923428297892,7.22132034));
#5612=CARTESIAN_POINT('Origin',(6.5,-5.73205080756888,7.28132034));
#5613=CARTESIAN_POINT('Origin',(9.5,-4.,7.22132034));
#5614=CARTESIAN_POINT('',(9.27,-4.32726136343907,7.28132034));
#5615=CARTESIAN_POINT('',(9.27,-4.32726136343907,8.48132034));
#5616=CARTESIAN_POINT('',(9.27,-4.32726136343907,7.22132034));
#5617=CARTESIAN_POINT('',(9.27,-3.67273863656093,7.28132034));
#5618=CARTESIAN_POINT('Origin',(9.5,-4.,7.28132034));
#5619=CARTESIAN_POINT('',(9.27,-3.67273863656093,8.48132034));
#5620=CARTESIAN_POINT('',(9.27,-3.67273863656093,7.22132034));
#5621=CARTESIAN_POINT('Origin',(9.5,-4.,8.48132034));
#5622=CARTESIAN_POINT('Origin',(8.5,-2.26794919243112,7.22132034));
#5623=CARTESIAN_POINT('',(8.10158334558463,-2.30350435358201,8.48132034));
#5624=CARTESIAN_POINT('',(8.10158334558463,-2.30350435358201,7.28132034));
#5625=CARTESIAN_POINT('',(8.10158334558463,-2.30350435358201,7.22132034));
#5626=CARTESIAN_POINT('',(8.66841665441537,-2.63076571702108,8.48132034));
#5627=CARTESIAN_POINT('Origin',(8.5,-2.26794919243112,8.48132034));
#5628=CARTESIAN_POINT('',(8.66841665441537,-2.63076571702108,7.28132034));
#5629=CARTESIAN_POINT('',(8.66841665441537,-2.63076571702108,7.22132034));
#5630=CARTESIAN_POINT('Origin',(8.5,-2.26794919243112,7.28132034));
#5631=CARTESIAN_POINT('Origin',(6.5,-2.26794919243112,7.22132034));
#5632=CARTESIAN_POINT('',(6.33158334558463,-2.63076571702108,8.48132034));
#5633=CARTESIAN_POINT('',(6.33158334558463,-2.63076571702108,7.28132034));
#5634=CARTESIAN_POINT('',(6.33158334558463,-2.63076571702108,7.22132034));
#5635=CARTESIAN_POINT('',(6.89841665441537,-2.30350435358201,8.48132034));
#5636=CARTESIAN_POINT('Origin',(6.5,-2.26794919243112,8.48132034));
#5637=CARTESIAN_POINT('',(6.89841665441537,-2.30350435358201,7.28132034));
#5638=CARTESIAN_POINT('',(6.89841665441537,-2.30350435358201,7.22132034));
#5639=CARTESIAN_POINT('Origin',(6.5,-2.26794919243112,7.28132034));
#5640=CARTESIAN_POINT('Origin',(5.5,-4.,7.22132034));
#5641=CARTESIAN_POINT('',(5.73,-4.32726136343907,8.48132034));
#5642=CARTESIAN_POINT('',(5.73,-4.32726136343907,7.28132034));
#5643=CARTESIAN_POINT('',(5.73,-4.32726136343907,7.22132034));
#5644=CARTESIAN_POINT('',(5.73,-3.67273863656093,8.48132034));
#5645=CARTESIAN_POINT('Origin',(5.5,-4.,8.48132034));
#5646=CARTESIAN_POINT('',(5.73,-3.67273863656093,7.28132034));
#5647=CARTESIAN_POINT('',(5.73,-3.67273863656093,7.22132034));
#5648=CARTESIAN_POINT('Origin',(5.5,-4.,7.28132034));
#5649=CARTESIAN_POINT('Origin',(8.5,-5.73205080756888,7.22132034));
#5650=CARTESIAN_POINT('',(8.66841665441537,-5.36923428297892,8.48132034));
#5651=CARTESIAN_POINT('',(8.66841665441537,-5.36923428297892,7.28132034));
#5652=CARTESIAN_POINT('',(8.66841665441537,-5.36923428297892,7.22132034));
#5653=CARTESIAN_POINT('',(8.10158334558463,-5.69649564641799,8.48132034));
#5654=CARTESIAN_POINT('Origin',(8.5,-5.73205080756888,8.48132034));
#5655=CARTESIAN_POINT('',(8.10158334558463,-5.69649564641799,7.28132034));
#5656=CARTESIAN_POINT('',(8.10158334558463,-5.69649564641799,7.22132034));
#5657=CARTESIAN_POINT('Origin',(8.5,-5.73205080756888,7.28132034));
#5658=CARTESIAN_POINT('Origin',(7.5,-4.,8.48132034));
#5659=CARTESIAN_POINT('Origin',(7.5,-4.,8.48132034));
#5660=CARTESIAN_POINT('Origin',(7.5,-4.,8.48132034));
#5661=CARTESIAN_POINT('Origin',(7.5,-4.,8.48132034));
#5662=CARTESIAN_POINT('Origin',(7.5,-4.,8.48132034));
#5663=CARTESIAN_POINT('Origin',(7.5,-4.,8.48132034));
#5664=CARTESIAN_POINT('Origin',(7.5,-4.,8.48132034));
#5665=CARTESIAN_POINT('',(7.075,-4.,8.48132034));
#5666=CARTESIAN_POINT('Origin',(7.5,-4.,8.48132034));
#5667=CARTESIAN_POINT('Origin',(7.5,-4.,7.28132034));
#5668=CARTESIAN_POINT('Origin',(7.5,-4.,7.28132034));
#5669=CARTESIAN_POINT('Origin',(7.5,-4.,7.28132034));
#5670=CARTESIAN_POINT('Origin',(7.5,-4.,7.28132034));
#5671=CARTESIAN_POINT('Origin',(7.5,-4.,7.28132034));
#5672=CARTESIAN_POINT('Origin',(7.5,-4.,7.28132034));
#5673=CARTESIAN_POINT('Origin',(7.5,-4.,7.28132034));
#5674=CARTESIAN_POINT('Origin',(7.5,-4.,7.28132034));
#5675=CARTESIAN_POINT('Origin',(7.5,-4.,7.28132034));
#5676=CARTESIAN_POINT('Origin',(7.5,-4.,7.28132034));
#5677=CARTESIAN_POINT('Origin',(7.5,-4.,7.28132034));
#5678=CARTESIAN_POINT('Origin',(7.5,-4.,7.28132034));
#5679=CARTESIAN_POINT('Origin',(7.87527767497326,-3.35,7.27132034));
#5680=CARTESIAN_POINT('',(7.87527767497326,-3.35,7.28132034));
#5681=CARTESIAN_POINT('',(7.12472232502674,-3.35,7.28132034));
#5682=CARTESIAN_POINT('',(7.68763883748663,-3.35,7.28132034));
#5683=CARTESIAN_POINT('',(7.87527767497326,-3.35,7.97132034));
#5684=CARTESIAN_POINT('',(7.87527767497326,-3.35,7.27132034));
#5685=CARTESIAN_POINT('',(7.12472232502674,-3.35,7.97132034));
#5686=CARTESIAN_POINT('',(7.87527767497326,-3.35,7.97132034));
#5687=CARTESIAN_POINT('',(7.12472232502674,-3.35,7.27132034));
#5688=CARTESIAN_POINT('Origin',(7.12472232502674,-3.35,7.27132034));
#5689=CARTESIAN_POINT('',(6.74944465005349,-4.,7.28132034));
#5690=CARTESIAN_POINT('',(7.03090290628343,-3.5125,7.28132034));
#5691=CARTESIAN_POINT('',(6.74944465005349,-4.,7.97132034));
#5692=CARTESIAN_POINT('',(7.12472232502674,-3.35,7.97132034));
#5693=CARTESIAN_POINT('',(6.74944465005349,-4.,7.27132034));
#5694=CARTESIAN_POINT('Origin',(6.74944465005349,-4.,7.27132034));
#5695=CARTESIAN_POINT('',(7.12472232502674,-4.65,7.28132034));
#5696=CARTESIAN_POINT('',(6.8432640687968,-4.1625,7.28132034));
#5697=CARTESIAN_POINT('',(7.12472232502674,-4.65,7.97132034));
#5698=CARTESIAN_POINT('',(6.74944465005349,-4.,7.97132034));
#5699=CARTESIAN_POINT('',(7.12472232502674,-4.65,7.27132034));
#5700=CARTESIAN_POINT('Origin',(7.12472232502674,-4.65,7.27132034));
#5701=CARTESIAN_POINT('',(7.87527767497326,-4.65,7.28132034));
#5702=CARTESIAN_POINT('',(7.31236116251337,-4.65,7.28132034));
#5703=CARTESIAN_POINT('',(7.87527767497326,-4.65,7.97132034));
#5704=CARTESIAN_POINT('',(7.12472232502674,-4.65,7.97132034));
#5705=CARTESIAN_POINT('',(7.87527767497326,-4.65,7.27132034));
#5706=CARTESIAN_POINT('Origin',(8.25055534994651,-4.,7.27132034));
#5707=CARTESIAN_POINT('',(8.25055534994651,-4.,7.28132034));
#5708=CARTESIAN_POINT('',(8.1567359312032,-3.8375,7.28132034));
#5709=CARTESIAN_POINT('',(8.25055534994651,-4.,7.97132034));
#5710=CARTESIAN_POINT('',(8.25055534994651,-4.,7.27132034));
#5711=CARTESIAN_POINT('',(8.25055534994651,-4.,7.97132034));
#5712=CARTESIAN_POINT('Origin',(7.87527767497326,-4.65,7.27132034));
#5713=CARTESIAN_POINT('',(7.96909709371657,-4.4875,7.28132034));
#5714=CARTESIAN_POINT('',(7.87527767497326,-4.65,7.97132034));
#5715=CARTESIAN_POINT('Origin',(7.5,-4.,7.97132034));
#5716=CARTESIAN_POINT('',(7.075,-4.,7.97132034));
#5717=CARTESIAN_POINT('Origin',(7.5,-4.,7.97132034));
#5718=CARTESIAN_POINT('Origin',(7.5,-4.,7.28132034));
#5719=CARTESIAN_POINT('',(7.075,-4.,7.28132034));
#5720=CARTESIAN_POINT('Origin',(7.5,-4.,7.28132034));
#5744=UNCERTAINTY_MEASURE_WITH_UNIT(LENGTH_MEASURE(0.001),#5762,
'DISTANCE_ACCURACY_VALUE',
'Maximum model space distance between geometric entities at asserted c
onnectivities');
#5745=UNCERTAINTY_MEASURE_WITH_UNIT(LENGTH_MEASURE(0.001),#5762,
'DISTANCE_ACCURACY_VALUE',
'Maximum model space distance between geometric entities at asserted c
onnectivities');
#5760=(
GEOMETRIC_REPRESENTATION_CONTEXT(3)
GLOBAL_UNCERTAINTY_ASSIGNED_CONTEXT((#5744))
GLOBAL_UNIT_ASSIGNED_CONTEXT((#5762,#5764,#5765))
REPRESENTATION_CONTEXT('','3D')
);
#5761=(
GEOMETRIC_REPRESENTATION_CONTEXT(3)
GLOBAL_UNCERTAINTY_ASSIGNED_CONTEXT((#5745))
GLOBAL_UNIT_ASSIGNED_CONTEXT((#5762,#5764,#5765))
REPRESENTATION_CONTEXT('','3D')
);
#5762=(
LENGTH_UNIT()
NAMED_UNIT(*)
SI_UNIT(.CENTI.,.METRE.)
);
#5764=(
NAMED_UNIT(*)
PLANE_ANGLE_UNIT()
SI_UNIT($,.RADIAN.)
);
#5765=(
NAMED_UNIT(*)
SI_UNIT($,.STERADIAN.)
SOLID_ANGLE_UNIT()
);
#5780=SHAPE_DEFINITION_REPRESENTATION(#5805,#5829);
#5805=PRODUCT_DEFINITION_SHAPE('',$,#5845);
#5829=SHAPE_REPRESENTATION('',(#3729),#5760);
#5830=PRODUCT_DEFINITION_CONTEXT('part definition',#5877,'design');
#5845=PRODUCT_DEFINITION('Captive-nut hand knob',
'Captive-nut hand knob',#5860,#5830);
#5860=PRODUCT_DEFINITION_FORMATION('',$,#5893);
#5877=APPLICATION_CONTEXT(
'Core Data for Automotive Mechanical Design Process');
#5878=PRODUCT_CONTEXT('part definition',#5877,'mechanical');
#5893=PRODUCT('Captive-nut hand knob','Captive-nut hand knob',
'Captive-nut hand knob',(#5878));
#5950=COLOUR_RGB('Black',0.12,0.14,0.17);
#5951=FILL_AREA_STYLE_COLOUR('',#5950);
#5952=FILL_AREA_STYLE('',(#5951));
#5953=SURFACE_STYLE_FILL_AREA(#5952);
#5954=SURFACE_SIDE_STYLE('',(#5953));
#5955=SURFACE_STYLE_USAGE(.BOTH.,#5954);
#5956=PRESENTATION_STYLE_ASSIGNMENT((#5955));
ENDSEC;
END-ISO-10303-21;
